ISO-10303-21;
HEADER;
/* Generated by software containing ST-Developer
 * from STEP Tools, Inc. (www.steptools.com) 
 */

FILE_DESCRIPTION(
/* description */ (''),
/* implementation_level */ '2;1');

FILE_NAME(
/* name */ 'Roller Carriage Spindle Nut.step',
/* time_stamp */ '2026-10-15T14:42:47-07:00',
/* author */ (''),
/* organization */ (''),
/* preprocessor_version */ 'ST-DEVELOPER v20.2',
/* originating_system */ 'Autodesk Translation Framework v15.15.0.0',
/* authorisation */ '');

FILE_SCHEMA (('AUTOMOTIVE_DESIGN { 1 0 10303 214 3 1 1 }'));
ENDSEC;

DATA;
#10=MECHANICAL_DESIGN_GEOMETRIC_PRESENTATION_REPRESENTATION('',(#239),#85789);
#203=SHAPE_REPRESENTATION_RELATIONSHIP('SRR','None',#85868,#221);
#221=ADVANCED_BREP_SHAPE_REPRESENTATION('',(#257),#85776);
#239=STYLED_ITEM('',(#85967),#257);
#257=MANIFOLD_SOLID_BREP('Body1',#9886);
#440=FACE_BOUND('',#3246,.T.);
#441=FACE_BOUND('',#3257,.T.);
#442=FACE_BOUND('',#3258,.T.);
#443=FACE_BOUND('',#3265,.T.);
#444=FACE_BOUND('',#3269,.T.);
#445=FACE_BOUND('',#3270,.T.);
#446=FACE_BOUND('',#3272,.T.);
#447=FACE_BOUND('',#3273,.T.);
#448=FACE_BOUND('',#3275,.T.);
#895=B_SPLINE_CURVE_WITH_KNOTS('',3,(#75815,#75816,#75817,#75818,#75819,
#75820,#75821,#75822,#75823,#75824,#75825,#75826),.UNSPECIFIED.,.F.,.F.,
(4,2,2,2,2,4),(-1.91155738203844,-1.85120908901733,-1.79086079599622,-1.670164209954,
-1.55191612324141,-1.43366803652883),.UNSPECIFIED.);
#896=B_SPLINE_CURVE_WITH_KNOTS('',3,(#75828,#75829,#75830,#75831,#75832,
#75833,#75834,#75835,#75836,#75837,#75838,#75839),.UNSPECIFIED.,.F.,.F.,
(4,2,2,2,2,4),(-0.477889345509609,-0.359641258797025,-0.24139317208444,
-0.12069658604222,-0.06034829302111,0.),.UNSPECIFIED.);
#897=B_SPLINE_CURVE_WITH_KNOTS('',3,(#75840,#75841,#75842,#75843,#75844,
#75845,#75846,#75847,#75848,#75849,#75850,#75851,#75852,#75853,#75854,#75855,
#75856,#75857,#75858,#75859,#75860,#75861),.UNSPECIFIED.,.F.,.F.,(4,2,2,
2,2,2,2,2,2,2,4),(-1.43366803652883,-1.31541994981624,-1.19717186310366,
-1.07647527706144,-1.01612698404033,-0.955778691019219,-0.895430397998109,
-0.835082104976999,-0.714385518934779,-0.596137432222194,-0.477889345509609),
 .UNSPECIFIED.);
#898=B_SPLINE_CURVE_WITH_KNOTS('',3,(#75865,#75866,#75867,#75868,#75869,
#75870,#75871,#75872,#75873,#75874,#75875,#75876,#75877,#75878,#75879,#75880,
#75881,#75882,#75883,#75884,#75885,#75886,#75887,#75888,#75889,#75890,#75891,
#75892,#75893,#75894,#75895,#75896),.UNSPECIFIED.,.F.,.F.,(4,2,2,2,2,2,
2,2,2,2,2,2,2,2,2,4),(-1.91155738203844,-1.85120908901733,-1.79086079599622,
-1.670164209954,-1.55191612324141,-1.43366803652883,-1.31541994981624,-1.19717186310366,
-1.07647527706144,-1.01612698404033,-0.955778691019219,-0.895430397998109,
-0.835082104976999,-0.714385518934779,-0.596137432222194,-0.47788934550961),
 .UNSPECIFIED.);
#899=B_SPLINE_CURVE_WITH_KNOTS('',3,(#75897,#75898,#75899,#75900,#75901,
#75902,#75903,#75904,#75905,#75906,#75907,#75908),.UNSPECIFIED.,.F.,.F.,
(4,2,2,2,2,4),(-0.47788934550961,-0.359641258797025,-0.241393172084441,
-0.12069658604222,-0.0603482930211102,0.),.UNSPECIFIED.);
#900=B_SPLINE_CURVE_WITH_KNOTS('',3,(#75918,#75919,#75920,#75921,#75922,
#75923,#75924,#75925,#75926,#75927),.UNSPECIFIED.,.F.,.F.,(4,2,2,2,4),(-1.22969838857394,
-1.15274028568534,-1.07578218279674,-0.9990279871136,-0.922273791430456),
 .UNSPECIFIED.);
#901=B_SPLINE_CURVE_WITH_KNOTS('',3,(#75929,#75930,#75931,#75932,#75933,
#75934,#75935,#75936,#75937,#75938),.UNSPECIFIED.,.F.,.F.,(4,2,2,2,4),(-0.307424597143485,
-0.230670401460341,-0.153916205777197,-0.0769581028885983,0.),
 .UNSPECIFIED.);
#902=B_SPLINE_CURVE_WITH_KNOTS('',3,(#75939,#75940,#75941,#75942,#75943,
#75944,#75945,#75946,#75947,#75948,#75949,#75950,#75951,#75952,#75953,#75954,
#75955,#75956),.UNSPECIFIED.,.F.,.F.,(4,2,2,2,2,2,2,2,4),(-0.922273791430456,
-0.845519595747312,-0.768765400064167,-0.691807297175569,-0.614849194286971,
-0.537891091398373,-0.460932988509774,-0.38417879282663,-0.307424597143485),
 .UNSPECIFIED.);
#903=B_SPLINE_CURVE_WITH_KNOTS('',3,(#75960,#75961,#75962,#75963,#75964,
#75965,#75966,#75967,#75968,#75969,#75970,#75971,#75972,#75973,#75974,#75975,
#75976,#75977,#75978,#75979,#75980,#75981,#75982,#75983,#75984,#75985),
 .UNSPECIFIED.,.F.,.F.,(4,2,2,2,2,2,2,2,2,2,2,2,4),(-1.22969838857394,-1.15274028568534,
-1.07578218279674,-0.9990279871136,-0.922273791430456,-0.845519595747312,
-0.768765400064167,-0.691807297175569,-0.614849194286971,-0.537891091398373,
-0.460932988509774,-0.38417879282663,-0.307424597143485),.UNSPECIFIED.);
#904=B_SPLINE_CURVE_WITH_KNOTS('',3,(#75986,#75987,#75988,#75989,#75990,
#75991,#75992,#75993,#75994,#75995),.UNSPECIFIED.,.F.,.F.,(4,2,2,2,4),(-0.307424597143485,
-0.230670401460341,-0.153916205777197,-0.0769581028885983,0.),
 .UNSPECIFIED.);
#1091=PLANE('',#10509);
#1092=PLANE('',#10515);
#1093=PLANE('',#10520);
#1094=PLANE('',#10526);
#1095=PLANE('',#10527);
#1096=PLANE('',#10528);
#1097=PLANE('',#10529);
#1098=PLANE('',#10530);
#1099=PLANE('',#10531);
#1100=PLANE('',#10543);
#1101=PLANE('',#10546);
#1102=PLANE('',#10548);
#1103=PLANE('',#10550);
#1104=PLANE('',#10556);
#1105=PLANE('',#10557);
#1106=PLANE('',#10558);
#1107=PLANE('',#10559);
#1108=PLANE('',#10560);
#1109=PLANE('',#10561);
#1489=LINE('',#75731,#2025);
#1490=LINE('',#75735,#2026);
#1491=LINE('',#75740,#2027);
#1492=LINE('',#75748,#2028);
#1493=LINE('',#75751,#2029);
#1494=LINE('',#75753,#2030);
#1495=LINE('',#75754,#2031);
#1496=LINE('',#75760,#2032);
#1497=LINE('',#75764,#2033);
#1498=LINE('',#75769,#2034);
#1499=LINE('',#75777,#2035);
#1500=LINE('',#75780,#2036);
#1501=LINE('',#75782,#2037);
#1502=LINE('',#75783,#2038);
#1503=LINE('',#75786,#2039);
#1504=LINE('',#75788,#2040);
#1505=LINE('',#75790,#2041);
#1506=LINE('',#75791,#2042);
#1507=LINE('',#75794,#2043);
#1508=LINE('',#75796,#2044);
#1509=LINE('',#75797,#2045);
#1510=LINE('',#75800,#2046);
#1511=LINE('',#75801,#2047);
#1512=LINE('',#75804,#2048);
#1513=LINE('',#75805,#2049);
#1514=LINE('',#75807,#2050);
#1515=LINE('',#75813,#2051);
#1516=LINE('',#75910,#2052);
#1517=LINE('',#75916,#2053);
#1518=LINE('',#75997,#2054);
#1519=LINE('',#76002,#2055);
#1520=LINE('',#76003,#2056);
#1521=LINE('',#76005,#2057);
#1522=LINE('',#76009,#2058);
#1523=LINE('',#76017,#2059);
#1524=LINE('',#76024,#2060);
#1525=LINE('',#76029,#2061);
#1526=LINE('',#76031,#2062);
#1527=LINE('',#76033,#2063);
#1528=LINE('',#76035,#2064);
#2025=VECTOR('',#12067,1.);
#2026=VECTOR('',#12070,1.);
#2027=VECTOR('',#12077,1.);
#2028=VECTOR('',#12084,1.);
#2029=VECTOR('',#12087,1.);
#2030=VECTOR('',#12090,1.);
#2031=VECTOR('',#12091,1.);
#2032=VECTOR('',#12096,1.);
#2033=VECTOR('',#12099,1.);
#2034=VECTOR('',#12106,1.);
#2035=VECTOR('',#12113,1.);
#2036=VECTOR('',#12116,1.);
#2037=VECTOR('',#12119,1.);
#2038=VECTOR('',#12120,1.);
#2039=VECTOR('',#12121,1.);
#2040=VECTOR('',#12122,1.);
#2041=VECTOR('',#12123,1.);
#2042=VECTOR('',#12124,1.);
#2043=VECTOR('',#12127,1.);
#2044=VECTOR('',#12128,1.);
#2045=VECTOR('',#12129,1.);
#2046=VECTOR('',#12132,1.);
#2047=VECTOR('',#12133,1.);
#2048=VECTOR('',#12136,1.);
#2049=VECTOR('',#12137,1.);
#2050=VECTOR('',#12140,1.);
#2051=VECTOR('',#12147,0.3);
#2052=VECTOR('',#12150,0.3);
#2053=VECTOR('',#12157,0.199999999999999);
#2054=VECTOR('',#12160,0.199999999999999);
#2055=VECTOR('',#12167,0.4025);
#2056=VECTOR('',#12168,0.4025);
#2057=VECTOR('',#12169,0.4025);
#2058=VECTOR('',#12174,1.);
#2059=VECTOR('',#12185,1.);
#2060=VECTOR('',#12196,1.1);
#2061=VECTOR('',#12205,1.);
#2062=VECTOR('',#12208,1.);
#2063=VECTOR('',#12211,1.);
#2064=VECTOR('',#12214,1.);
#2328=CYLINDRICAL_SURFACE('',#10505,0.15);
#2329=CYLINDRICAL_SURFACE('',#10511,0.15);
#2330=CYLINDRICAL_SURFACE('',#10516,0.15);
#2331=CYLINDRICAL_SURFACE('',#10522,0.15);
#2332=CYLINDRICAL_SURFACE('',#10532,0.3);
#2333=CYLINDRICAL_SURFACE('',#10534,0.3);
#2334=CYLINDRICAL_SURFACE('',#10536,0.199999999999999);
#2335=CYLINDRICAL_SURFACE('',#10538,0.199999999999999);
#2336=CYLINDRICAL_SURFACE('',#10540,0.4025);
#2337=CYLINDRICAL_SURFACE('',#10552,1.1);
#2683=FACE_OUTER_BOUND('',#3238,.T.);
#2684=FACE_OUTER_BOUND('',#3239,.T.);
#2685=FACE_OUTER_BOUND('',#3240,.T.);
#2686=FACE_OUTER_BOUND('',#3241,.T.);
#2687=FACE_OUTER_BOUND('',#3242,.T.);
#2688=FACE_OUTER_BOUND('',#3243,.T.);
#2689=FACE_OUTER_BOUND('',#3244,.T.);
#2690=FACE_OUTER_BOUND('',#3245,.T.);
#2691=FACE_OUTER_BOUND('',#3247,.T.);
#2692=FACE_OUTER_BOUND('',#3248,.T.);
#2693=FACE_OUTER_BOUND('',#3249,.T.);
#2694=FACE_OUTER_BOUND('',#3250,.T.);
#2695=FACE_OUTER_BOUND('',#3251,.T.);
#2696=FACE_OUTER_BOUND('',#3252,.T.);
#2697=FACE_OUTER_BOUND('',#3253,.T.);
#2698=FACE_OUTER_BOUND('',#3254,.T.);
#2699=FACE_OUTER_BOUND('',#3255,.T.);
#2700=FACE_OUTER_BOUND('',#3256,.T.);
#2701=FACE_OUTER_BOUND('',#3259,.T.);
#2702=FACE_OUTER_BOUND('',#3260,.T.);
#2703=FACE_OUTER_BOUND('',#3261,.T.);
#2704=FACE_OUTER_BOUND('',#3262,.T.);
#2705=FACE_OUTER_BOUND('',#3263,.T.);
#2706=FACE_OUTER_BOUND('',#3264,.T.);
#2707=FACE_OUTER_BOUND('',#3266,.T.);
#2708=FACE_OUTER_BOUND('',#3267,.T.);
#2709=FACE_OUTER_BOUND('',#3268,.T.);
#2710=FACE_OUTER_BOUND('',#3271,.T.);
#2711=FACE_OUTER_BOUND('',#3274,.T.);
#3238=EDGE_LOOP('',(#8249,#8250,#8251,#8252,#8253));
#3239=EDGE_LOOP('',(#8254,#8255,#8256));
#3240=EDGE_LOOP('',(#8257,#8258,#8259,#8260,#8261));
#3241=EDGE_LOOP('',(#8262,#8263,#8264,#8265));
#3242=EDGE_LOOP('',(#8266,#8267,#8268,#8269,#8270));
#3243=EDGE_LOOP('',(#8271,#8272,#8273));
#3244=EDGE_LOOP('',(#8274,#8275,#8276,#8277,#8278));
#3245=EDGE_LOOP('',(#8279,#8280,#8281,#8282));
#3246=EDGE_LOOP('',(#8283,#8284,#8285,#8286));
#3247=EDGE_LOOP('',(#8287,#8288,#8289,#8290));
#3248=EDGE_LOOP('',(#8291,#8292,#8293,#8294));
#3249=EDGE_LOOP('',(#8295,#8296,#8297,#8298));
#3250=EDGE_LOOP('',(#8299,#8300,#8301,#8302));
#3251=EDGE_LOOP('',(#8303,#8304,#8305,#8306));
#3252=EDGE_LOOP('',(#8307,#8308,#8309,#8310,#8311,#8312));
#3253=EDGE_LOOP('',(#8313,#8314,#8315,#8316,#8317));
#3254=EDGE_LOOP('',(#8318,#8319,#8320,#8321,#8322,#8323));
#3255=EDGE_LOOP('',(#8324,#8325,#8326,#8327,#8328));
#3256=EDGE_LOOP('',(#8329,#8330,#8331,#8332,#8333,#8334,#8335,#8336,#8337,
#8338,#8339,#8340,#8341,#8342));
#3257=EDGE_LOOP('',(#8343,#8344));
#3258=EDGE_LOOP('',(#8345,#8346));
#3259=EDGE_LOOP('',(#8347,#8348,#8349));
#3260=EDGE_LOOP('',(#8350,#8351,#8352,#8353));
#3261=EDGE_LOOP('',(#8354,#8355));
#3262=EDGE_LOOP('',(#8356,#8357,#8358,#8359));
#3263=EDGE_LOOP('',(#8360,#8361,#8362,#8363,#8364,#8365,#8366,#8367,#8368,
#8369,#8370,#8371));
#3264=EDGE_LOOP('',(#8372));
#3265=EDGE_LOOP('',(#8373));
#3266=EDGE_LOOP('',(#8374,#8375,#8376));
#3267=EDGE_LOOP('',(#8377,#8378,#8379));
#3268=EDGE_LOOP('',(#8380,#8381,#8382,#8383,#8384,#8385));
#3269=EDGE_LOOP('',(#8386));
#3270=EDGE_LOOP('',(#8387));
#3271=EDGE_LOOP('',(#8388,#8389,#8390,#8391,#8392,#8393));
#3272=EDGE_LOOP('',(#8394));
#3273=EDGE_LOOP('',(#8395));
#3274=EDGE_LOOP('',(#8396,#8397,#8398,#8399,#8400,#8401,#8402,#8403));
#3275=EDGE_LOOP('',(#8404));
#3700=CIRCLE('',#10506,0.15);
#3701=CIRCLE('',#10507,0.15);
#3702=CIRCLE('',#10508,0.15);
#3703=CIRCLE('',#10510,1.1);
#3704=CIRCLE('',#10512,0.15);
#3705=CIRCLE('',#10513,0.15);
#3706=CIRCLE('',#10514,0.15);
#3707=CIRCLE('',#10517,0.15);
#3708=CIRCLE('',#10518,0.15);
#3709=CIRCLE('',#10519,0.15);
#3710=CIRCLE('',#10521,1.1);
#3711=CIRCLE('',#10523,0.15);
#3712=CIRCLE('',#10524,0.15);
#3713=CIRCLE('',#10525,0.15);
#3714=CIRCLE('',#10533,0.3);
#3715=CIRCLE('',#10535,0.3);
#3716=CIRCLE('',#10537,0.199999999999999);
#3717=CIRCLE('',#10539,0.199999999999999);
#3718=CIRCLE('',#10541,0.4025);
#3719=CIRCLE('',#10542,0.4025);
#3720=CIRCLE('',#10544,1.1);
#3721=CIRCLE('',#10545,1.1);
#3722=CIRCLE('',#10547,1.1);
#3723=CIRCLE('',#10549,1.1);
#3724=CIRCLE('',#10551,1.1);
#3725=CIRCLE('',#10553,1.1);
#3726=CIRCLE('',#10554,1.1);
#3727=CIRCLE('',#10555,1.1);
#4551=VERTEX_POINT('',#75727);
#4552=VERTEX_POINT('',#75728);
#4553=VERTEX_POINT('',#75730);
#4554=VERTEX_POINT('',#75732);
#4555=VERTEX_POINT('',#75734);
#4556=VERTEX_POINT('',#75738);
#4557=VERTEX_POINT('',#75742);
#4558=VERTEX_POINT('',#75743);
#4559=VERTEX_POINT('',#75745);
#4560=VERTEX_POINT('',#75747);
#4561=VERTEX_POINT('',#75749);
#4562=VERTEX_POINT('',#75756);
#4563=VERTEX_POINT('',#75757);
#4564=VERTEX_POINT('',#75759);
#4565=VERTEX_POINT('',#75761);
#4566=VERTEX_POINT('',#75763);
#4567=VERTEX_POINT('',#75767);
#4568=VERTEX_POINT('',#75771);
#4569=VERTEX_POINT('',#75772);
#4570=VERTEX_POINT('',#75774);
#4571=VERTEX_POINT('',#75776);
#4572=VERTEX_POINT('',#75778);
#4573=VERTEX_POINT('',#75784);
#4574=VERTEX_POINT('',#75785);
#4575=VERTEX_POINT('',#75787);
#4576=VERTEX_POINT('',#75789);
#4577=VERTEX_POINT('',#75793);
#4578=VERTEX_POINT('',#75795);
#4579=VERTEX_POINT('',#75799);
#4580=VERTEX_POINT('',#75803);
#4581=VERTEX_POINT('',#75810);
#4582=VERTEX_POINT('',#75812);
#4583=VERTEX_POINT('',#75814);
#4584=VERTEX_POINT('',#75827);
#4585=VERTEX_POINT('',#75863);
#4586=VERTEX_POINT('',#75864);
#4587=VERTEX_POINT('',#75909);
#4588=VERTEX_POINT('',#75913);
#4589=VERTEX_POINT('',#75915);
#4590=VERTEX_POINT('',#75917);
#4591=VERTEX_POINT('',#75928);
#4592=VERTEX_POINT('',#75958);
#4593=VERTEX_POINT('',#75959);
#4594=VERTEX_POINT('',#75996);
#4595=VERTEX_POINT('',#76000);
#4596=VERTEX_POINT('',#76004);
#4597=VERTEX_POINT('',#76008);
#4598=VERTEX_POINT('',#76010);
#4599=VERTEX_POINT('',#76016);
#4600=VERTEX_POINT('',#76022);
#5852=EDGE_CURVE('',#4551,#4552,#3700,.T.);
#5853=EDGE_CURVE('',#4552,#4553,#1489,.T.);
#5854=EDGE_CURVE('',#4553,#4554,#3701,.T.);
#5855=EDGE_CURVE('',#4554,#4555,#1490,.T.);
#5856=EDGE_CURVE('',#4555,#4551,#3702,.F.);
#5857=EDGE_CURVE('',#4551,#4556,#3703,.T.);
#5858=EDGE_CURVE('',#4556,#4552,#1491,.T.);
#5859=EDGE_CURVE('',#4557,#4558,#3704,.T.);
#5860=EDGE_CURVE('',#4559,#4558,#3705,.T.);
#5861=EDGE_CURVE('',#4559,#4560,#1492,.T.);
#5862=EDGE_CURVE('',#4560,#4561,#3706,.T.);
#5863=EDGE_CURVE('',#4561,#4557,#1493,.T.);
#5864=EDGE_CURVE('',#4554,#4560,#1494,.T.);
#5865=EDGE_CURVE('',#4555,#4559,#1495,.T.);
#5866=EDGE_CURVE('',#4562,#4563,#3707,.T.);
#5867=EDGE_CURVE('',#4563,#4564,#1496,.T.);
#5868=EDGE_CURVE('',#4564,#4565,#3708,.T.);
#5869=EDGE_CURVE('',#4565,#4566,#1497,.T.);
#5870=EDGE_CURVE('',#4566,#4562,#3709,.F.);
#5871=EDGE_CURVE('',#4562,#4567,#3710,.T.);
#5872=EDGE_CURVE('',#4567,#4563,#1498,.T.);
#5873=EDGE_CURVE('',#4568,#4569,#3711,.T.);
#5874=EDGE_CURVE('',#4570,#4569,#3712,.T.);
#5875=EDGE_CURVE('',#4570,#4571,#1499,.T.);
#5876=EDGE_CURVE('',#4571,#4572,#3713,.T.);
#5877=EDGE_CURVE('',#4572,#4568,#1500,.T.);
#5878=EDGE_CURVE('',#4565,#4571,#1501,.T.);
#5879=EDGE_CURVE('',#4566,#4570,#1502,.T.);
#5880=EDGE_CURVE('',#4573,#4574,#1503,.T.);
#5881=EDGE_CURVE('',#4574,#4575,#1504,.T.);
#5882=EDGE_CURVE('',#4575,#4576,#1505,.T.);
#5883=EDGE_CURVE('',#4576,#4573,#1506,.T.);
#5884=EDGE_CURVE('',#4573,#4577,#1507,.T.);
#5885=EDGE_CURVE('',#4577,#4578,#1508,.T.);
#5886=EDGE_CURVE('',#4574,#4578,#1509,.T.);
#5887=EDGE_CURVE('',#4576,#4579,#1510,.T.);
#5888=EDGE_CURVE('',#4579,#4577,#1511,.T.);
#5889=EDGE_CURVE('',#4575,#4580,#1512,.T.);
#5890=EDGE_CURVE('',#4580,#4579,#1513,.T.);
#5891=EDGE_CURVE('',#4578,#4580,#1514,.T.);
#5892=EDGE_CURVE('',#4581,#4581,#3714,.T.);
#5893=EDGE_CURVE('',#4581,#4582,#1515,.T.);
#5894=EDGE_CURVE('',#4583,#4582,#895,.T.);
#5895=EDGE_CURVE('',#4584,#4583,#896,.T.);
#5896=EDGE_CURVE('',#4582,#4584,#897,.T.);
#5897=EDGE_CURVE('',#4585,#4586,#898,.T.);
#5898=EDGE_CURVE('',#4586,#4585,#899,.T.);
#5899=EDGE_CURVE('',#4586,#4587,#1516,.T.);
#5900=EDGE_CURVE('',#4587,#4587,#3715,.T.);
#5901=EDGE_CURVE('',#4588,#4588,#3716,.T.);
#5902=EDGE_CURVE('',#4588,#4589,#1517,.T.);
#5903=EDGE_CURVE('',#4590,#4589,#900,.T.);
#5904=EDGE_CURVE('',#4591,#4590,#901,.T.);
#5905=EDGE_CURVE('',#4589,#4591,#902,.T.);
#5906=EDGE_CURVE('',#4592,#4593,#903,.T.);
#5907=EDGE_CURVE('',#4593,#4592,#904,.T.);
#5908=EDGE_CURVE('',#4593,#4594,#1518,.T.);
#5909=EDGE_CURVE('',#4594,#4594,#3717,.T.);
#5910=EDGE_CURVE('',#4595,#4595,#3718,.T.);
#5911=EDGE_CURVE('',#4595,#4589,#1519,.T.);
#5912=EDGE_CURVE('',#4591,#4582,#1520,.T.);
#5913=EDGE_CURVE('',#4584,#4596,#1521,.T.);
#5914=EDGE_CURVE('',#4596,#4596,#3719,.T.);
#5915=EDGE_CURVE('',#4597,#4556,#1522,.T.);
#5916=EDGE_CURVE('',#4598,#4556,#3720,.T.);
#5917=EDGE_CURVE('',#4597,#4598,#3721,.T.);
#5918=EDGE_CURVE('',#4558,#4551,#3722,.T.);
#5919=EDGE_CURVE('',#4599,#4567,#1523,.T.);
#5920=EDGE_CURVE('',#4599,#4567,#3723,.T.);
#5921=EDGE_CURVE('',#4569,#4562,#3724,.T.);
#5922=EDGE_CURVE('',#4600,#4600,#3725,.T.);
#5923=EDGE_CURVE('',#4600,#4598,#1524,.T.);
#5924=EDGE_CURVE('',#4599,#4558,#3726,.T.);
#5925=EDGE_CURVE('',#4597,#4569,#3727,.T.);
#5926=EDGE_CURVE('',#4557,#4599,#1525,.T.);
#5927=EDGE_CURVE('',#4568,#4597,#1526,.T.);
#5928=EDGE_CURVE('',#4561,#4564,#1527,.T.);
#5929=EDGE_CURVE('',#4572,#4553,#1528,.T.);
#8249=ORIENTED_EDGE('',*,*,#5852,.T.);
#8250=ORIENTED_EDGE('',*,*,#5853,.T.);
#8251=ORIENTED_EDGE('',*,*,#5854,.T.);
#8252=ORIENTED_EDGE('',*,*,#5855,.T.);
#8253=ORIENTED_EDGE('',*,*,#5856,.T.);
#8254=ORIENTED_EDGE('',*,*,#5852,.F.);
#8255=ORIENTED_EDGE('',*,*,#5857,.T.);
#8256=ORIENTED_EDGE('',*,*,#5858,.T.);
#8257=ORIENTED_EDGE('',*,*,#5859,.T.);
#8258=ORIENTED_EDGE('',*,*,#5860,.F.);
#8259=ORIENTED_EDGE('',*,*,#5861,.T.);
#8260=ORIENTED_EDGE('',*,*,#5862,.T.);
#8261=ORIENTED_EDGE('',*,*,#5863,.T.);
#8262=ORIENTED_EDGE('',*,*,#5855,.F.);
#8263=ORIENTED_EDGE('',*,*,#5864,.T.);
#8264=ORIENTED_EDGE('',*,*,#5861,.F.);
#8265=ORIENTED_EDGE('',*,*,#5865,.F.);
#8266=ORIENTED_EDGE('',*,*,#5866,.T.);
#8267=ORIENTED_EDGE('',*,*,#5867,.T.);
#8268=ORIENTED_EDGE('',*,*,#5868,.T.);
#8269=ORIENTED_EDGE('',*,*,#5869,.T.);
#8270=ORIENTED_EDGE('',*,*,#5870,.T.);
#8271=ORIENTED_EDGE('',*,*,#5866,.F.);
#8272=ORIENTED_EDGE('',*,*,#5871,.T.);
#8273=ORIENTED_EDGE('',*,*,#5872,.T.);
#8274=ORIENTED_EDGE('',*,*,#5873,.T.);
#8275=ORIENTED_EDGE('',*,*,#5874,.F.);
#8276=ORIENTED_EDGE('',*,*,#5875,.T.);
#8277=ORIENTED_EDGE('',*,*,#5876,.T.);
#8278=ORIENTED_EDGE('',*,*,#5877,.T.);
#8279=ORIENTED_EDGE('',*,*,#5869,.F.);
#8280=ORIENTED_EDGE('',*,*,#5878,.T.);
#8281=ORIENTED_EDGE('',*,*,#5875,.F.);
#8282=ORIENTED_EDGE('',*,*,#5879,.F.);
#8283=ORIENTED_EDGE('',*,*,#5880,.T.);
#8284=ORIENTED_EDGE('',*,*,#5881,.T.);
#8285=ORIENTED_EDGE('',*,*,#5882,.T.);
#8286=ORIENTED_EDGE('',*,*,#5883,.T.);
#8287=ORIENTED_EDGE('',*,*,#5880,.F.);
#8288=ORIENTED_EDGE('',*,*,#5884,.T.);
#8289=ORIENTED_EDGE('',*,*,#5885,.T.);
#8290=ORIENTED_EDGE('',*,*,#5886,.F.);
#8291=ORIENTED_EDGE('',*,*,#5883,.F.);
#8292=ORIENTED_EDGE('',*,*,#5887,.T.);
#8293=ORIENTED_EDGE('',*,*,#5888,.T.);
#8294=ORIENTED_EDGE('',*,*,#5884,.F.);
#8295=ORIENTED_EDGE('',*,*,#5882,.F.);
#8296=ORIENTED_EDGE('',*,*,#5889,.T.);
#8297=ORIENTED_EDGE('',*,*,#5890,.T.);
#8298=ORIENTED_EDGE('',*,*,#5887,.F.);
#8299=ORIENTED_EDGE('',*,*,#5881,.F.);
#8300=ORIENTED_EDGE('',*,*,#5886,.T.);
#8301=ORIENTED_EDGE('',*,*,#5891,.T.);
#8302=ORIENTED_EDGE('',*,*,#5889,.F.);
#8303=ORIENTED_EDGE('',*,*,#5891,.F.);
#8304=ORIENTED_EDGE('',*,*,#5885,.F.);
#8305=ORIENTED_EDGE('',*,*,#5888,.F.);
#8306=ORIENTED_EDGE('',*,*,#5890,.F.);
#8307=ORIENTED_EDGE('',*,*,#5892,.F.);
#8308=ORIENTED_EDGE('',*,*,#5893,.T.);
#8309=ORIENTED_EDGE('',*,*,#5894,.F.);
#8310=ORIENTED_EDGE('',*,*,#5895,.F.);
#8311=ORIENTED_EDGE('',*,*,#5896,.F.);
#8312=ORIENTED_EDGE('',*,*,#5893,.F.);
#8313=ORIENTED_EDGE('',*,*,#5897,.F.);
#8314=ORIENTED_EDGE('',*,*,#5898,.F.);
#8315=ORIENTED_EDGE('',*,*,#5899,.T.);
#8316=ORIENTED_EDGE('',*,*,#5900,.F.);
#8317=ORIENTED_EDGE('',*,*,#5899,.F.);
#8318=ORIENTED_EDGE('',*,*,#5901,.F.);
#8319=ORIENTED_EDGE('',*,*,#5902,.T.);
#8320=ORIENTED_EDGE('',*,*,#5903,.F.);
#8321=ORIENTED_EDGE('',*,*,#5904,.F.);
#8322=ORIENTED_EDGE('',*,*,#5905,.F.);
#8323=ORIENTED_EDGE('',*,*,#5902,.F.);
#8324=ORIENTED_EDGE('',*,*,#5906,.F.);
#8325=ORIENTED_EDGE('',*,*,#5907,.F.);
#8326=ORIENTED_EDGE('',*,*,#5908,.T.);
#8327=ORIENTED_EDGE('',*,*,#5909,.F.);
#8328=ORIENTED_EDGE('',*,*,#5908,.F.);
#8329=ORIENTED_EDGE('',*,*,#5910,.F.);
#8330=ORIENTED_EDGE('',*,*,#5911,.T.);
#8331=ORIENTED_EDGE('',*,*,#5905,.T.);
#8332=ORIENTED_EDGE('',*,*,#5912,.T.);
#8333=ORIENTED_EDGE('',*,*,#5896,.T.);
#8334=ORIENTED_EDGE('',*,*,#5913,.T.);
#8335=ORIENTED_EDGE('',*,*,#5914,.F.);
#8336=ORIENTED_EDGE('',*,*,#5913,.F.);
#8337=ORIENTED_EDGE('',*,*,#5895,.T.);
#8338=ORIENTED_EDGE('',*,*,#5894,.T.);
#8339=ORIENTED_EDGE('',*,*,#5912,.F.);
#8340=ORIENTED_EDGE('',*,*,#5904,.T.);
#8341=ORIENTED_EDGE('',*,*,#5903,.T.);
#8342=ORIENTED_EDGE('',*,*,#5911,.F.);
#8343=ORIENTED_EDGE('',*,*,#5897,.T.);
#8344=ORIENTED_EDGE('',*,*,#5898,.T.);
#8345=ORIENTED_EDGE('',*,*,#5906,.T.);
#8346=ORIENTED_EDGE('',*,*,#5907,.T.);
#8347=ORIENTED_EDGE('',*,*,#5915,.T.);
#8348=ORIENTED_EDGE('',*,*,#5916,.F.);
#8349=ORIENTED_EDGE('',*,*,#5917,.F.);
#8350=ORIENTED_EDGE('',*,*,#5865,.T.);
#8351=ORIENTED_EDGE('',*,*,#5860,.T.);
#8352=ORIENTED_EDGE('',*,*,#5918,.T.);
#8353=ORIENTED_EDGE('',*,*,#5856,.F.);
#8354=ORIENTED_EDGE('',*,*,#5919,.T.);
#8355=ORIENTED_EDGE('',*,*,#5920,.F.);
#8356=ORIENTED_EDGE('',*,*,#5879,.T.);
#8357=ORIENTED_EDGE('',*,*,#5874,.T.);
#8358=ORIENTED_EDGE('',*,*,#5921,.T.);
#8359=ORIENTED_EDGE('',*,*,#5870,.F.);
#8360=ORIENTED_EDGE('',*,*,#5922,.F.);
#8361=ORIENTED_EDGE('',*,*,#5923,.T.);
#8362=ORIENTED_EDGE('',*,*,#5916,.T.);
#8363=ORIENTED_EDGE('',*,*,#5857,.F.);
#8364=ORIENTED_EDGE('',*,*,#5918,.F.);
#8365=ORIENTED_EDGE('',*,*,#5924,.F.);
#8366=ORIENTED_EDGE('',*,*,#5920,.T.);
#8367=ORIENTED_EDGE('',*,*,#5871,.F.);
#8368=ORIENTED_EDGE('',*,*,#5921,.F.);
#8369=ORIENTED_EDGE('',*,*,#5925,.F.);
#8370=ORIENTED_EDGE('',*,*,#5917,.T.);
#8371=ORIENTED_EDGE('',*,*,#5923,.F.);
#8372=ORIENTED_EDGE('',*,*,#5922,.T.);
#8373=ORIENTED_EDGE('',*,*,#5910,.T.);
#8374=ORIENTED_EDGE('',*,*,#5859,.F.);
#8375=ORIENTED_EDGE('',*,*,#5926,.T.);
#8376=ORIENTED_EDGE('',*,*,#5924,.T.);
#8377=ORIENTED_EDGE('',*,*,#5873,.F.);
#8378=ORIENTED_EDGE('',*,*,#5927,.T.);
#8379=ORIENTED_EDGE('',*,*,#5925,.T.);
#8380=ORIENTED_EDGE('',*,*,#5863,.F.);
#8381=ORIENTED_EDGE('',*,*,#5928,.T.);
#8382=ORIENTED_EDGE('',*,*,#5867,.F.);
#8383=ORIENTED_EDGE('',*,*,#5872,.F.);
#8384=ORIENTED_EDGE('',*,*,#5919,.F.);
#8385=ORIENTED_EDGE('',*,*,#5926,.F.);
#8386=ORIENTED_EDGE('',*,*,#5900,.T.);
#8387=ORIENTED_EDGE('',*,*,#5909,.T.);
#8388=ORIENTED_EDGE('',*,*,#5853,.F.);
#8389=ORIENTED_EDGE('',*,*,#5858,.F.);
#8390=ORIENTED_EDGE('',*,*,#5915,.F.);
#8391=ORIENTED_EDGE('',*,*,#5927,.F.);
#8392=ORIENTED_EDGE('',*,*,#5877,.F.);
#8393=ORIENTED_EDGE('',*,*,#5929,.T.);
#8394=ORIENTED_EDGE('',*,*,#5892,.T.);
#8395=ORIENTED_EDGE('',*,*,#5901,.T.);
#8396=ORIENTED_EDGE('',*,*,#5854,.F.);
#8397=ORIENTED_EDGE('',*,*,#5929,.F.);
#8398=ORIENTED_EDGE('',*,*,#5876,.F.);
#8399=ORIENTED_EDGE('',*,*,#5878,.F.);
#8400=ORIENTED_EDGE('',*,*,#5868,.F.);
#8401=ORIENTED_EDGE('',*,*,#5928,.F.);
#8402=ORIENTED_EDGE('',*,*,#5862,.F.);
#8403=ORIENTED_EDGE('',*,*,#5864,.F.);
#8404=ORIENTED_EDGE('',*,*,#5914,.T.);
#9661=ADVANCED_FACE('',(#2683),#2328,.T.);
#9662=ADVANCED_FACE('',(#2684),#1091,.T.);
#9663=ADVANCED_FACE('',(#2685),#2329,.T.);
#9664=ADVANCED_FACE('',(#2686),#1092,.T.);
#9665=ADVANCED_FACE('',(#2687),#2330,.T.);
#9666=ADVANCED_FACE('',(#2688),#1093,.T.);
#9667=ADVANCED_FACE('',(#2689),#2331,.T.);
#9668=ADVANCED_FACE('',(#2690,#440),#1094,.T.);
#9669=ADVANCED_FACE('',(#2691),#1095,.F.);
#9670=ADVANCED_FACE('',(#2692),#1096,.F.);
#9671=ADVANCED_FACE('',(#2693),#1097,.F.);
#9672=ADVANCED_FACE('',(#2694),#1098,.F.);
#9673=ADVANCED_FACE('',(#2695),#1099,.F.);
#9674=ADVANCED_FACE('',(#2696),#2332,.F.);
#9675=ADVANCED_FACE('',(#2697),#2333,.F.);
#9676=ADVANCED_FACE('',(#2698),#2334,.F.);
#9677=ADVANCED_FACE('',(#2699),#2335,.F.);
#9678=ADVANCED_FACE('',(#2700,#441,#442),#2336,.F.);
#9679=ADVANCED_FACE('',(#2701),#1100,.F.);
#9680=ADVANCED_FACE('',(#2702),#1101,.F.);
#9681=ADVANCED_FACE('',(#2703),#1102,.F.);
#9682=ADVANCED_FACE('',(#2704),#1103,.F.);
#9683=ADVANCED_FACE('',(#2705),#2337,.T.);
#9684=ADVANCED_FACE('',(#2706,#443),#1104,.T.);
#9685=ADVANCED_FACE('',(#2707),#1105,.T.);
#9686=ADVANCED_FACE('',(#2708),#1106,.T.);
#9687=ADVANCED_FACE('',(#2709,#444,#445),#1107,.T.);
#9688=ADVANCED_FACE('',(#2710,#446,#447),#1108,.T.);
#9689=ADVANCED_FACE('',(#2711,#448),#1109,.F.);
#9886=CLOSED_SHELL('',(#9661,#9662,#9663,#9664,#9665,#9666,#9667,#9668,
#9669,#9670,#9671,#9672,#9673,#9674,#9675,#9676,#9677,#9678,#9679,#9680,
#9681,#9682,#9683,#9684,#9685,#9686,#9687,#9688,#9689));
#10504=AXIS2_PLACEMENT_3D('',#75725,#12061,#12062);
#10505=AXIS2_PLACEMENT_3D('',#75726,#12063,#12064);
#10506=AXIS2_PLACEMENT_3D('',#75729,#12065,#12066);
#10507=AXIS2_PLACEMENT_3D('',#75733,#12068,#12069);
#10508=AXIS2_PLACEMENT_3D('',#75736,#12071,#12072);
#10509=AXIS2_PLACEMENT_3D('',#75737,#12073,#12074);
#10510=AXIS2_PLACEMENT_3D('',#75739,#12075,#12076);
#10511=AXIS2_PLACEMENT_3D('',#75741,#12078,#12079);
#10512=AXIS2_PLACEMENT_3D('',#75744,#12080,#12081);
#10513=AXIS2_PLACEMENT_3D('',#75746,#12082,#12083);
#10514=AXIS2_PLACEMENT_3D('',#75750,#12085,#12086);
#10515=AXIS2_PLACEMENT_3D('',#75752,#12088,#12089);
#10516=AXIS2_PLACEMENT_3D('',#75755,#12092,#12093);
#10517=AXIS2_PLACEMENT_3D('',#75758,#12094,#12095);
#10518=AXIS2_PLACEMENT_3D('',#75762,#12097,#12098);
#10519=AXIS2_PLACEMENT_3D('',#75765,#12100,#12101);
#10520=AXIS2_PLACEMENT_3D('',#75766,#12102,#12103);
#10521=AXIS2_PLACEMENT_3D('',#75768,#12104,#12105);
#10522=AXIS2_PLACEMENT_3D('',#75770,#12107,#12108);
#10523=AXIS2_PLACEMENT_3D('',#75773,#12109,#12110);
#10524=AXIS2_PLACEMENT_3D('',#75775,#12111,#12112);
#10525=AXIS2_PLACEMENT_3D('',#75779,#12114,#12115);
#10526=AXIS2_PLACEMENT_3D('',#75781,#12117,#12118);
#10527=AXIS2_PLACEMENT_3D('',#75792,#12125,#12126);
#10528=AXIS2_PLACEMENT_3D('',#75798,#12130,#12131);
#10529=AXIS2_PLACEMENT_3D('',#75802,#12134,#12135);
#10530=AXIS2_PLACEMENT_3D('',#75806,#12138,#12139);
#10531=AXIS2_PLACEMENT_3D('',#75808,#12141,#12142);
#10532=AXIS2_PLACEMENT_3D('',#75809,#12143,#12144);
#10533=AXIS2_PLACEMENT_3D('',#75811,#12145,#12146);
#10534=AXIS2_PLACEMENT_3D('',#75862,#12148,#12149);
#10535=AXIS2_PLACEMENT_3D('',#75911,#12151,#12152);
#10536=AXIS2_PLACEMENT_3D('',#75912,#12153,#12154);
#10537=AXIS2_PLACEMENT_3D('',#75914,#12155,#12156);
#10538=AXIS2_PLACEMENT_3D('',#75957,#12158,#12159);
#10539=AXIS2_PLACEMENT_3D('',#75998,#12161,#12162);
#10540=AXIS2_PLACEMENT_3D('',#75999,#12163,#12164);
#10541=AXIS2_PLACEMENT_3D('',#76001,#12165,#12166);
#10542=AXIS2_PLACEMENT_3D('',#76006,#12170,#12171);
#10543=AXIS2_PLACEMENT_3D('',#76007,#12172,#12173);
#10544=AXIS2_PLACEMENT_3D('',#76011,#12175,#12176);
#10545=AXIS2_PLACEMENT_3D('',#76012,#12177,#12178);
#10546=AXIS2_PLACEMENT_3D('',#76013,#12179,#12180);
#10547=AXIS2_PLACEMENT_3D('',#76014,#12181,#12182);
#10548=AXIS2_PLACEMENT_3D('',#76015,#12183,#12184);
#10549=AXIS2_PLACEMENT_3D('',#76018,#12186,#12187);
#10550=AXIS2_PLACEMENT_3D('',#76019,#12188,#12189);
#10551=AXIS2_PLACEMENT_3D('',#76020,#12190,#12191);
#10552=AXIS2_PLACEMENT_3D('',#76021,#12192,#12193);
#10553=AXIS2_PLACEMENT_3D('',#76023,#12194,#12195);
#10554=AXIS2_PLACEMENT_3D('',#76025,#12197,#12198);
#10555=AXIS2_PLACEMENT_3D('',#76026,#12199,#12200);
#10556=AXIS2_PLACEMENT_3D('',#76027,#12201,#12202);
#10557=AXIS2_PLACEMENT_3D('',#76028,#12203,#12204);
#10558=AXIS2_PLACEMENT_3D('',#76030,#12206,#12207);
#10559=AXIS2_PLACEMENT_3D('',#76032,#12209,#12210);
#10560=AXIS2_PLACEMENT_3D('',#76034,#12212,#12213);
#10561=AXIS2_PLACEMENT_3D('',#76036,#12215,#12216);
#12061=DIRECTION('axis',(0.,0.,1.));
#12062=DIRECTION('refdir',(1.,0.,0.));
#12063=DIRECTION('center_axis',(0.,0.,1.));
#12064=DIRECTION('ref_axis',(-0.707106781186546,-0.707106781186549,0.));
#12065=DIRECTION('center_axis',(0.,0.,-1.));
#12066=DIRECTION('ref_axis',(-0.707106781186546,-0.707106781186549,0.));
#12067=DIRECTION('',(0.,0.,-1.));
#12068=DIRECTION('center_axis',(0.,0.,1.));
#12069=DIRECTION('ref_axis',(-0.707106781186546,-0.707106781186549,0.));
#12070=DIRECTION('',(0.,0.,1.));
#12071=DIRECTION('center_axis',(0.,0.,1.));
#12072=DIRECTION('ref_axis',(-0.707106781186546,-0.707106781186549,0.));
#12073=DIRECTION('center_axis',(0.,0.,1.));
#12074=DIRECTION('ref_axis',(1.,0.,0.));
#12075=DIRECTION('center_axis',(0.,0.,-1.));
#12076=DIRECTION('ref_axis',(1.,0.,0.));
#12077=DIRECTION('',(0.,-1.,0.));
#12078=DIRECTION('center_axis',(0.,0.,1.));
#12079=DIRECTION('ref_axis',(0.707106781186546,-0.707106781186549,0.));
#12080=DIRECTION('center_axis',(0.,0.,-1.));
#12081=DIRECTION('ref_axis',(0.707106781186546,-0.707106781186549,0.));
#12082=DIRECTION('center_axis',(0.,0.,1.));
#12083=DIRECTION('ref_axis',(0.707106781186546,-0.707106781186549,0.));
#12084=DIRECTION('',(0.,0.,-1.));
#12085=DIRECTION('center_axis',(0.,0.,1.));
#12086=DIRECTION('ref_axis',(0.707106781186546,-0.707106781186549,0.));
#12087=DIRECTION('',(0.,0.,1.));
#12088=DIRECTION('center_axis',(0.,-1.,0.));
#12089=DIRECTION('ref_axis',(1.,0.,0.));
#12090=DIRECTION('',(1.,0.,0.));
#12091=DIRECTION('',(1.,0.,0.));
#12092=DIRECTION('center_axis',(0.,0.,1.));
#12093=DIRECTION('ref_axis',(0.707106781186546,0.707106781186549,0.));
#12094=DIRECTION('center_axis',(0.,0.,-1.));
#12095=DIRECTION('ref_axis',(0.707106781186546,0.707106781186549,0.));
#12096=DIRECTION('',(0.,0.,-1.));
#12097=DIRECTION('center_axis',(0.,0.,1.));
#12098=DIRECTION('ref_axis',(0.707106781186546,0.707106781186549,0.));
#12099=DIRECTION('',(0.,0.,1.));
#12100=DIRECTION('center_axis',(0.,0.,1.));
#12101=DIRECTION('ref_axis',(0.707106781186546,0.707106781186549,0.));
#12102=DIRECTION('center_axis',(0.,0.,1.));
#12103=DIRECTION('ref_axis',(1.,0.,0.));
#12104=DIRECTION('center_axis',(0.,0.,-1.));
#12105=DIRECTION('ref_axis',(1.,0.,0.));
#12106=DIRECTION('',(0.,1.,0.));
#12107=DIRECTION('center_axis',(0.,0.,1.));
#12108=DIRECTION('ref_axis',(-0.707106781186546,0.707106781186549,0.));
#12109=DIRECTION('center_axis',(0.,0.,-1.));
#12110=DIRECTION('ref_axis',(-0.707106781186546,0.707106781186549,0.));
#12111=DIRECTION('center_axis',(0.,0.,1.));
#12112=DIRECTION('ref_axis',(-0.707106781186546,0.707106781186549,0.));
#12113=DIRECTION('',(0.,0.,-1.));
#12114=DIRECTION('center_axis',(0.,0.,1.));
#12115=DIRECTION('ref_axis',(-0.707106781186546,0.707106781186549,0.));
#12116=DIRECTION('',(0.,0.,1.));
#12117=DIRECTION('center_axis',(0.,1.,0.));
#12118=DIRECTION('ref_axis',(-1.,0.,0.));
#12119=DIRECTION('',(-1.,0.,0.));
#12120=DIRECTION('',(-1.,0.,0.));
#12121=DIRECTION('',(0.,0.,1.));
#12122=DIRECTION('',(-1.,0.,0.));
#12123=DIRECTION('',(0.,0.,-1.));
#12124=DIRECTION('',(1.,0.,0.));
#12125=DIRECTION('center_axis',(1.,0.,0.));
#12126=DIRECTION('ref_axis',(0.,0.,1.));
#12127=DIRECTION('',(0.,-1.,0.));
#12128=DIRECTION('',(0.,0.,1.));
#12129=DIRECTION('',(0.,-1.,0.));
#12130=DIRECTION('center_axis',(0.,0.,-1.));
#12131=DIRECTION('ref_axis',(1.,0.,0.));
#12132=DIRECTION('',(0.,-1.,0.));
#12133=DIRECTION('',(1.,0.,0.));
#12134=DIRECTION('center_axis',(-1.,0.,0.));
#12135=DIRECTION('ref_axis',(0.,0.,-1.));
#12136=DIRECTION('',(0.,-1.,0.));
#12137=DIRECTION('',(0.,0.,-1.));
#12138=DIRECTION('center_axis',(0.,0.,1.));
#12139=DIRECTION('ref_axis',(-1.,0.,0.));
#12140=DIRECTION('',(-1.,0.,0.));
#12141=DIRECTION('center_axis',(0.,-1.,0.));
#12142=DIRECTION('ref_axis',(0.,0.,-1.));
#12143=DIRECTION('center_axis',(1.,0.,0.));
#12144=DIRECTION('ref_axis',(0.,0.,-1.));
#12145=DIRECTION('center_axis',(1.,0.,0.));
#12146=DIRECTION('ref_axis',(0.,0.,-1.));
#12147=DIRECTION('',(1.,0.,0.));
#12148=DIRECTION('center_axis',(1.,0.,0.));
#12149=DIRECTION('ref_axis',(0.,0.,-1.));
#12150=DIRECTION('',(1.,0.,0.));
#12151=DIRECTION('center_axis',(-1.,0.,0.));
#12152=DIRECTION('ref_axis',(0.,0.,-1.));
#12153=DIRECTION('center_axis',(1.,0.,0.));
#12154=DIRECTION('ref_axis',(0.,0.,-1.));
#12155=DIRECTION('center_axis',(1.,0.,0.));
#12156=DIRECTION('ref_axis',(0.,0.,-1.));
#12157=DIRECTION('',(1.,0.,0.));
#12158=DIRECTION('center_axis',(1.,0.,0.));
#12159=DIRECTION('ref_axis',(0.,0.,-1.));
#12160=DIRECTION('',(1.,0.,0.));
#12161=DIRECTION('center_axis',(-1.,0.,0.));
#12162=DIRECTION('ref_axis',(0.,0.,-1.));
#12163=DIRECTION('center_axis',(0.,0.,-1.));
#12164=DIRECTION('ref_axis',(1.,0.,0.));
#12165=DIRECTION('center_axis',(0.,0.,-1.));
#12166=DIRECTION('ref_axis',(1.,0.,0.));
#12167=DIRECTION('',(0.,0.,-1.));
#12168=DIRECTION('',(0.,0.,-1.));
#12169=DIRECTION('',(0.,0.,-1.));
#12170=DIRECTION('center_axis',(0.,0.,1.));
#12171=DIRECTION('ref_axis',(1.,0.,0.));
#12172=DIRECTION('center_axis',(0.,0.,1.));
#12173=DIRECTION('ref_axis',(1.,0.,0.));
#12174=DIRECTION('',(0.,-1.,0.));
#12175=DIRECTION('center_axis',(0.,0.,1.));
#12176=DIRECTION('ref_axis',(1.,0.,0.));
#12177=DIRECTION('center_axis',(0.,0.,1.));
#12178=DIRECTION('ref_axis',(1.,0.,0.));
#12179=DIRECTION('center_axis',(0.,0.,1.));
#12180=DIRECTION('ref_axis',(1.,0.,0.));
#12181=DIRECTION('center_axis',(0.,0.,-1.));
#12182=DIRECTION('ref_axis',(1.,0.,0.));
#12183=DIRECTION('center_axis',(0.,0.,1.));
#12184=DIRECTION('ref_axis',(1.,0.,0.));
#12185=DIRECTION('',(0.,1.,0.));
#12186=DIRECTION('center_axis',(0.,0.,1.));
#12187=DIRECTION('ref_axis',(1.,0.,0.));
#12188=DIRECTION('center_axis',(0.,0.,1.));
#12189=DIRECTION('ref_axis',(1.,0.,0.));
#12190=DIRECTION('center_axis',(0.,0.,-1.));
#12191=DIRECTION('ref_axis',(1.,0.,0.));
#12192=DIRECTION('center_axis',(0.,0.,1.));
#12193=DIRECTION('ref_axis',(1.,0.,0.));
#12194=DIRECTION('center_axis',(0.,0.,1.));
#12195=DIRECTION('ref_axis',(1.,0.,0.));
#12196=DIRECTION('',(0.,0.,-1.));
#12197=DIRECTION('center_axis',(0.,0.,-1.));
#12198=DIRECTION('ref_axis',(1.,0.,0.));
#12199=DIRECTION('center_axis',(0.,0.,-1.));
#12200=DIRECTION('ref_axis',(1.,0.,0.));
#12201=DIRECTION('center_axis',(0.,0.,1.));
#12202=DIRECTION('ref_axis',(1.,0.,0.));
#12203=DIRECTION('center_axis',(0.,0.,1.));
#12204=DIRECTION('ref_axis',(1.,0.,0.));
#12205=DIRECTION('',(0.,1.,0.));
#12206=DIRECTION('center_axis',(0.,0.,1.));
#12207=DIRECTION('ref_axis',(1.,0.,0.));
#12208=DIRECTION('',(0.,-1.,0.));
#12209=DIRECTION('center_axis',(1.,0.,0.));
#12210=DIRECTION('ref_axis',(0.,1.,0.));
#12211=DIRECTION('',(0.,1.,0.));
#12212=DIRECTION('center_axis',(-1.,0.,0.));
#12213=DIRECTION('ref_axis',(0.,-1.,0.));
#12214=DIRECTION('',(0.,-1.,0.));
#12215=DIRECTION('center_axis',(0.,0.,1.));
#12216=DIRECTION('ref_axis',(1.,0.,0.));
#75725=CARTESIAN_POINT('',(0.,0.,0.));
#75726=CARTESIAN_POINT('Origin',(-0.75,1.45,6.));
#75727=CARTESIAN_POINT('',(-0.755074409108712,1.3000858566639,9.2));
#75728=CARTESIAN_POINT('',(-0.9,1.45,9.2));
#75729=CARTESIAN_POINT('Origin',(-0.75,1.45,9.2));
#75730=CARTESIAN_POINT('',(-0.9,1.45,6.));
#75731=CARTESIAN_POINT('',(-0.9,1.45,6.));
#75732=CARTESIAN_POINT('',(-0.75,1.3,6.));
#75733=CARTESIAN_POINT('Origin',(-0.75,1.45,6.));
#75734=CARTESIAN_POINT('',(-0.75,1.3,9.2));
#75735=CARTESIAN_POINT('',(-0.75,1.3,6.));
#75736=CARTESIAN_POINT('Origin',(-0.75,1.45,9.2));
#75737=CARTESIAN_POINT('Origin',(0.,2.1,9.2));
#75738=CARTESIAN_POINT('',(-0.9,1.46754446796632,9.2));
#75739=CARTESIAN_POINT('Origin',(0.,2.1,9.2));
#75740=CARTESIAN_POINT('',(-0.9,2.9,9.2));
#75741=CARTESIAN_POINT('Origin',(0.75,1.45,6.));
#75742=CARTESIAN_POINT('',(0.9,1.45,9.2));
#75743=CARTESIAN_POINT('',(0.755074409108712,1.3000858566639,9.2));
#75744=CARTESIAN_POINT('Origin',(0.75,1.45,9.2));
#75745=CARTESIAN_POINT('',(0.75,1.3,9.2));
#75746=CARTESIAN_POINT('Origin',(0.75,1.45,9.2));
#75747=CARTESIAN_POINT('',(0.75,1.3,6.));
#75748=CARTESIAN_POINT('',(0.75,1.3,6.));
#75749=CARTESIAN_POINT('',(0.9,1.45,6.));
#75750=CARTESIAN_POINT('Origin',(0.75,1.45,6.));
#75751=CARTESIAN_POINT('',(0.9,1.45,6.));
#75752=CARTESIAN_POINT('Origin',(-0.9,1.3,6.));
#75753=CARTESIAN_POINT('',(-0.9,1.3,6.));
#75754=CARTESIAN_POINT('',(-0.9,1.3,9.2));
#75755=CARTESIAN_POINT('Origin',(0.75,2.75,6.));
#75756=CARTESIAN_POINT('',(0.755074409108712,2.8999141433361,9.2));
#75757=CARTESIAN_POINT('',(0.9,2.75,9.2));
#75758=CARTESIAN_POINT('Origin',(0.75,2.75,9.2));
#75759=CARTESIAN_POINT('',(0.9,2.75,6.));
#75760=CARTESIAN_POINT('',(0.9,2.75,6.));
#75761=CARTESIAN_POINT('',(0.75,2.9,6.));
#75762=CARTESIAN_POINT('Origin',(0.75,2.75,6.));
#75763=CARTESIAN_POINT('',(0.75,2.9,9.2));
#75764=CARTESIAN_POINT('',(0.75,2.9,6.));
#75765=CARTESIAN_POINT('Origin',(0.75,2.75,9.2));
#75766=CARTESIAN_POINT('Origin',(0.,2.1,9.2));
#75767=CARTESIAN_POINT('',(0.9,2.73245553203368,9.2));
#75768=CARTESIAN_POINT('Origin',(0.,2.1,9.2));
#75769=CARTESIAN_POINT('',(0.9,1.3,9.2));
#75770=CARTESIAN_POINT('Origin',(-0.75,2.75,6.));
#75771=CARTESIAN_POINT('',(-0.9,2.75,9.2));
#75772=CARTESIAN_POINT('',(-0.755074409108712,2.8999141433361,9.2));
#75773=CARTESIAN_POINT('Origin',(-0.75,2.75,9.2));
#75774=CARTESIAN_POINT('',(-0.75,2.9,9.2));
#75775=CARTESIAN_POINT('Origin',(-0.75,2.75,9.2));
#75776=CARTESIAN_POINT('',(-0.75,2.9,6.));
#75777=CARTESIAN_POINT('',(-0.75,2.9,6.));
#75778=CARTESIAN_POINT('',(-0.9,2.75,6.));
#75779=CARTESIAN_POINT('Origin',(-0.75,2.75,6.));
#75780=CARTESIAN_POINT('',(-0.9,2.75,6.));
#75781=CARTESIAN_POINT('Origin',(0.9,2.9,6.));
#75782=CARTESIAN_POINT('',(0.9,2.9,6.));
#75783=CARTESIAN_POINT('',(0.9,2.9,9.2));
#75784=CARTESIAN_POINT('',(0.5,2.9,6.3));
#75785=CARTESIAN_POINT('',(0.5,2.9,6.9));
#75786=CARTESIAN_POINT('',(0.5,2.9,6.15));
#75787=CARTESIAN_POINT('',(-0.5,2.9,6.9));
#75788=CARTESIAN_POINT('',(0.7,2.9,6.9));
#75789=CARTESIAN_POINT('',(-0.5,2.9,6.3));
#75790=CARTESIAN_POINT('',(-0.5,2.9,6.45));
#75791=CARTESIAN_POINT('',(0.2,2.9,6.3));
#75792=CARTESIAN_POINT('Origin',(0.5,2.9,6.3));
#75793=CARTESIAN_POINT('',(0.5,2.6,6.3));
#75794=CARTESIAN_POINT('',(0.5,2.9,6.3));
#75795=CARTESIAN_POINT('',(0.5,2.6,6.9));
#75796=CARTESIAN_POINT('',(0.5,2.6,6.3));
#75797=CARTESIAN_POINT('',(0.5,2.9,6.9));
#75798=CARTESIAN_POINT('Origin',(-0.5,2.9,6.3));
#75799=CARTESIAN_POINT('',(-0.5,2.6,6.3));
#75800=CARTESIAN_POINT('',(-0.5,2.9,6.3));
#75801=CARTESIAN_POINT('',(-0.5,2.6,6.3));
#75802=CARTESIAN_POINT('Origin',(-0.5,2.9,6.9));
#75803=CARTESIAN_POINT('',(-0.5,2.6,6.9));
#75804=CARTESIAN_POINT('',(-0.5,2.9,6.9));
#75805=CARTESIAN_POINT('',(-0.5,2.6,6.9));
#75806=CARTESIAN_POINT('Origin',(0.5,2.9,6.9));
#75807=CARTESIAN_POINT('',(0.5,2.6,6.9));
#75808=CARTESIAN_POINT('Origin',(0.,2.6,6.6));
#75809=CARTESIAN_POINT('Origin',(-0.9,2.1,7.4));
#75810=CARTESIAN_POINT('',(-0.9,2.1,7.7));
#75811=CARTESIAN_POINT('Origin',(-0.9,2.1,7.4));
#75812=CARTESIAN_POINT('',(-0.4025,2.1,7.7));
#75813=CARTESIAN_POINT('',(-0.9,2.1,7.7));
#75814=CARTESIAN_POINT('',(-0.26833980323463,1.8,7.4));
#75815=CARTESIAN_POINT('Ctrl Pts',(-0.26833980323463,1.8,7.4));
#75816=CARTESIAN_POINT('Ctrl Pts',(-0.26833980323463,1.8,7.4201160976737));
#75817=CARTESIAN_POINT('Ctrl Pts',(-0.270671600644359,1.8020440352048,7.44032404072543));
#75818=CARTESIAN_POINT('Ctrl Pts',(-0.279265580045418,1.81008344690125,
7.47970055135893));
#75819=CARTESIAN_POINT('Ctrl Pts',(-0.285490508258182,1.81607405099208,
7.49887821451971));
#75820=CARTESIAN_POINT('Ctrl Pts',(-0.307328099584212,1.83922089052474,
7.55348515936485));
#75821=CARTESIAN_POINT('Ctrl Pts',(-0.325904486897266,1.86181444421644,
7.58607851292837));
#75822=CARTESIAN_POINT('Ctrl Pts',(-0.357891266971383,1.91339295489154,
7.63765702360347));
#75823=CARTESIAN_POINT('Ctrl Pts',(-0.373877283104246,1.94605224242681,
7.66056900592672));
#75824=CARTESIAN_POINT('Ctrl Pts',(-0.396259291153439,2.01960899212744,
7.69177630545863));
#75825=CARTESIAN_POINT('Ctrl Pts',(-0.4025,2.06058397109581,7.7));
#75826=CARTESIAN_POINT('Ctrl Pts',(-0.4025,2.1,7.7));
#75827=CARTESIAN_POINT('',(-0.4025,2.1,7.1));
#75828=CARTESIAN_POINT('Ctrl Pts',(-0.4025,2.1,7.1));
#75829=CARTESIAN_POINT('Ctrl Pts',(-0.4025,2.0605839710958,7.1));
#75830=CARTESIAN_POINT('Ctrl Pts',(-0.396259291153439,2.01960899212744,
7.10822369454137));
#75831=CARTESIAN_POINT('Ctrl Pts',(-0.373877283104246,1.94605224242681,
7.13943099407328));
#75832=CARTESIAN_POINT('Ctrl Pts',(-0.357891266971382,1.91339295489154,
7.16234297639653));
#75833=CARTESIAN_POINT('Ctrl Pts',(-0.325904486897266,1.86181444421644,
7.21392148707163));
#75834=CARTESIAN_POINT('Ctrl Pts',(-0.307328099584211,1.83922089052474,
7.24651484063515));
#75835=CARTESIAN_POINT('Ctrl Pts',(-0.285490508258181,1.81607405099208,
7.3011217854803));
#75836=CARTESIAN_POINT('Ctrl Pts',(-0.279265580045417,1.81008344690125,
7.32029944864107));
#75837=CARTESIAN_POINT('Ctrl Pts',(-0.270671600644359,1.8020440352048,7.35967595927457));
#75838=CARTESIAN_POINT('Ctrl Pts',(-0.26833980323463,1.8,7.3798839023263));
#75839=CARTESIAN_POINT('Ctrl Pts',(-0.26833980323463,1.8,7.4));
#75840=CARTESIAN_POINT('Ctrl Pts',(-0.4025,2.1,7.7));
#75841=CARTESIAN_POINT('Ctrl Pts',(-0.4025,2.1394160289042,7.7));
#75842=CARTESIAN_POINT('Ctrl Pts',(-0.396259291153439,2.18039100787256,
7.69177630545863));
#75843=CARTESIAN_POINT('Ctrl Pts',(-0.373877283104246,2.25394775757319,
7.66056900592672));
#75844=CARTESIAN_POINT('Ctrl Pts',(-0.357891266971382,2.28660704510846,
7.63765702360347));
#75845=CARTESIAN_POINT('Ctrl Pts',(-0.325904486897266,2.33818555578356,
7.58607851292837));
#75846=CARTESIAN_POINT('Ctrl Pts',(-0.307328099584212,2.36077910947526,
7.55348515936485));
#75847=CARTESIAN_POINT('Ctrl Pts',(-0.285490508258182,2.38392594900792,
7.49887821451971));
#75848=CARTESIAN_POINT('Ctrl Pts',(-0.279265580045418,2.38991655309875,
7.47970055135893));
#75849=CARTESIAN_POINT('Ctrl Pts',(-0.270671600644359,2.3979559647952,7.44032404072543));
#75850=CARTESIAN_POINT('Ctrl Pts',(-0.26833980323463,2.4,7.4201160976737));
#75851=CARTESIAN_POINT('Ctrl Pts',(-0.26833980323463,2.4,7.3798839023263));
#75852=CARTESIAN_POINT('Ctrl Pts',(-0.27067160064436,2.3979559647952,7.35967595927457));
#75853=CARTESIAN_POINT('Ctrl Pts',(-0.279265580045418,2.38991655309875,
7.32029944864107));
#75854=CARTESIAN_POINT('Ctrl Pts',(-0.285490508258181,2.38392594900792,
7.3011217854803));
#75855=CARTESIAN_POINT('Ctrl Pts',(-0.307328099584212,2.36077910947526,
7.24651484063515));
#75856=CARTESIAN_POINT('Ctrl Pts',(-0.325904486897266,2.33818555578356,
7.21392148707163));
#75857=CARTESIAN_POINT('Ctrl Pts',(-0.357891266971382,2.28660704510846,
7.16234297639653));
#75858=CARTESIAN_POINT('Ctrl Pts',(-0.373877283104246,2.25394775757319,
7.13943099407329));
#75859=CARTESIAN_POINT('Ctrl Pts',(-0.396259291153439,2.18039100787256,
7.10822369454138));
#75860=CARTESIAN_POINT('Ctrl Pts',(-0.4025,2.1394160289042,7.1));
#75861=CARTESIAN_POINT('Ctrl Pts',(-0.4025,2.1,7.1));
#75862=CARTESIAN_POINT('Origin',(-0.9,2.1,7.4));
#75863=CARTESIAN_POINT('',(0.26833980323463,1.8,7.4));
#75864=CARTESIAN_POINT('',(0.4025,2.1,7.7));
#75865=CARTESIAN_POINT('Ctrl Pts',(0.26833980323463,1.8,7.4));
#75866=CARTESIAN_POINT('Ctrl Pts',(0.26833980323463,1.8,7.3798839023263));
#75867=CARTESIAN_POINT('Ctrl Pts',(0.27067160064436,1.8020440352048,7.35967595927457));
#75868=CARTESIAN_POINT('Ctrl Pts',(0.279265580045418,1.81008344690125,7.32029944864107));
#75869=CARTESIAN_POINT('Ctrl Pts',(0.285490508258181,1.81607405099208,7.3011217854803));
#75870=CARTESIAN_POINT('Ctrl Pts',(0.307328099584211,1.83922089052474,7.24651484063515));
#75871=CARTESIAN_POINT('Ctrl Pts',(0.325904486897266,1.86181444421644,7.21392148707163));
#75872=CARTESIAN_POINT('Ctrl Pts',(0.357891266971382,1.91339295489154,7.16234297639653));
#75873=CARTESIAN_POINT('Ctrl Pts',(0.373877283104246,1.94605224242681,7.13943099407328));
#75874=CARTESIAN_POINT('Ctrl Pts',(0.396259291153439,2.01960899212744,7.10822369454137));
#75875=CARTESIAN_POINT('Ctrl Pts',(0.4025,2.0605839710958,7.1));
#75876=CARTESIAN_POINT('Ctrl Pts',(0.4025,2.1394160289042,7.1));
#75877=CARTESIAN_POINT('Ctrl Pts',(0.396259291153439,2.18039100787256,7.10822369454137));
#75878=CARTESIAN_POINT('Ctrl Pts',(0.373877283104246,2.25394775757319,7.13943099407328));
#75879=CARTESIAN_POINT('Ctrl Pts',(0.357891266971382,2.28660704510846,7.16234297639653));
#75880=CARTESIAN_POINT('Ctrl Pts',(0.325904486897266,2.33818555578356,7.21392148707163));
#75881=CARTESIAN_POINT('Ctrl Pts',(0.307328099584211,2.36077910947526,7.24651484063515));
#75882=CARTESIAN_POINT('Ctrl Pts',(0.285490508258181,2.38392594900792,7.3011217854803));
#75883=CARTESIAN_POINT('Ctrl Pts',(0.279265580045418,2.38991655309875,7.32029944864107));
#75884=CARTESIAN_POINT('Ctrl Pts',(0.27067160064436,2.3979559647952,7.35967595927456));
#75885=CARTESIAN_POINT('Ctrl Pts',(0.26833980323463,2.4,7.3798839023263));
#75886=CARTESIAN_POINT('Ctrl Pts',(0.26833980323463,2.4,7.4201160976737));
#75887=CARTESIAN_POINT('Ctrl Pts',(0.270671600644359,2.3979559647952,7.44032404072543));
#75888=CARTESIAN_POINT('Ctrl Pts',(0.279265580045417,2.38991655309875,7.47970055135893));
#75889=CARTESIAN_POINT('Ctrl Pts',(0.285490508258181,2.38392594900792,7.4988782145197));
#75890=CARTESIAN_POINT('Ctrl Pts',(0.307328099584211,2.36077910947526,7.55348515936485));
#75891=CARTESIAN_POINT('Ctrl Pts',(0.325904486897266,2.33818555578356,7.58607851292837));
#75892=CARTESIAN_POINT('Ctrl Pts',(0.357891266971382,2.28660704510846,7.63765702360347));
#75893=CARTESIAN_POINT('Ctrl Pts',(0.373877283104246,2.25394775757319,7.66056900592671));
#75894=CARTESIAN_POINT('Ctrl Pts',(0.396259291153439,2.18039100787256,7.69177630545863));
#75895=CARTESIAN_POINT('Ctrl Pts',(0.4025,2.1394160289042,7.7));
#75896=CARTESIAN_POINT('Ctrl Pts',(0.4025,2.1,7.7));
#75897=CARTESIAN_POINT('Ctrl Pts',(0.4025,2.1,7.7));
#75898=CARTESIAN_POINT('Ctrl Pts',(0.4025,2.06058397109581,7.7));
#75899=CARTESIAN_POINT('Ctrl Pts',(0.396259291153439,2.01960899212744,7.69177630545863));
#75900=CARTESIAN_POINT('Ctrl Pts',(0.373877283104246,1.94605224242681,7.66056900592672));
#75901=CARTESIAN_POINT('Ctrl Pts',(0.357891266971382,1.91339295489154,7.63765702360347));
#75902=CARTESIAN_POINT('Ctrl Pts',(0.325904486897266,1.86181444421644,7.58607851292837));
#75903=CARTESIAN_POINT('Ctrl Pts',(0.307328099584212,1.83922089052474,7.55348515936485));
#75904=CARTESIAN_POINT('Ctrl Pts',(0.285490508258182,1.81607405099208,7.49887821451971));
#75905=CARTESIAN_POINT('Ctrl Pts',(0.279265580045418,1.81008344690125,7.47970055135894));
#75906=CARTESIAN_POINT('Ctrl Pts',(0.27067160064436,1.8020440352048,7.44032404072544));
#75907=CARTESIAN_POINT('Ctrl Pts',(0.26833980323463,1.8,7.4201160976737));
#75908=CARTESIAN_POINT('Ctrl Pts',(0.26833980323463,1.8,7.4));
#75909=CARTESIAN_POINT('',(0.9,2.1,7.7));
#75910=CARTESIAN_POINT('',(-0.9,2.1,7.7));
#75911=CARTESIAN_POINT('Origin',(0.9,2.1,7.4));
#75912=CARTESIAN_POINT('Origin',(-0.9,2.1,8.8));
#75913=CARTESIAN_POINT('',(-0.9,2.1,9.));
#75914=CARTESIAN_POINT('Origin',(-0.9,2.1,8.8));
#75915=CARTESIAN_POINT('',(-0.4025,2.1,9.));
#75916=CARTESIAN_POINT('',(-0.9,2.1,9.));
#75917=CARTESIAN_POINT('',(-0.349293930665851,1.9,8.8));
#75918=CARTESIAN_POINT('Ctrl Pts',(-0.349293930665851,1.9,8.8));
#75919=CARTESIAN_POINT('Ctrl Pts',(-0.349293930665851,1.9,8.82565270096287));
#75920=CARTESIAN_POINT('Ctrl Pts',(-0.352420767781585,1.90521995494474,
8.85261753143099));
#75921=CARTESIAN_POINT('Ctrl Pts',(-0.36301047494859,1.92575005043977,8.9017095986343));
#75922=CARTESIAN_POINT('Ctrl Pts',(-0.370257522731817,1.94104625437123,
8.92388896684585));
#75923=CARTESIAN_POINT('Ctrl Pts',(-0.383399376780438,1.97606457955938,
8.958907292034));
#75924=CARTESIAN_POINT('Ctrl Pts',(-0.390233771050516,1.99825967753044,
8.97423762194434));
#75925=CARTESIAN_POINT('Ctrl Pts',(-0.399836030760712,2.04742017386295,
8.99479529221648));
#75926=CARTESIAN_POINT('Ctrl Pts',(-0.4025,2.07441526810562,9.));
#75927=CARTESIAN_POINT('Ctrl Pts',(-0.4025,2.1,9.));
#75928=CARTESIAN_POINT('',(-0.4025,2.1,8.6));
#75929=CARTESIAN_POINT('Ctrl Pts',(-0.4025,2.1,8.6));
#75930=CARTESIAN_POINT('Ctrl Pts',(-0.4025,2.07441526810562,8.6));
#75931=CARTESIAN_POINT('Ctrl Pts',(-0.399836030760712,2.04742017386295,
8.60520470778352));
#75932=CARTESIAN_POINT('Ctrl Pts',(-0.390233771050516,1.99825967753044,
8.62576237805566));
#75933=CARTESIAN_POINT('Ctrl Pts',(-0.383399376780438,1.97606457955938,
8.641092707966));
#75934=CARTESIAN_POINT('Ctrl Pts',(-0.370257522731817,1.94104625437123,
8.67611103315415));
#75935=CARTESIAN_POINT('Ctrl Pts',(-0.36301047494859,1.92575005043977,8.6982904013657));
#75936=CARTESIAN_POINT('Ctrl Pts',(-0.352420767781585,1.90521995494474,
8.74738246856901));
#75937=CARTESIAN_POINT('Ctrl Pts',(-0.349293930665851,1.9,8.77434729903714));
#75938=CARTESIAN_POINT('Ctrl Pts',(-0.349293930665851,1.9,8.8));
#75939=CARTESIAN_POINT('Ctrl Pts',(-0.4025,2.1,9.));
#75940=CARTESIAN_POINT('Ctrl Pts',(-0.4025,2.12558473189438,9.));
#75941=CARTESIAN_POINT('Ctrl Pts',(-0.399836030760712,2.15257982613705,
8.99479529221648));
#75942=CARTESIAN_POINT('Ctrl Pts',(-0.390233771050516,2.20174032246956,
8.97423762194434));
#75943=CARTESIAN_POINT('Ctrl Pts',(-0.383399376780438,2.22393542044062,
8.958907292034));
#75944=CARTESIAN_POINT('Ctrl Pts',(-0.370257522731817,2.25895374562877,
8.92388896684585));
#75945=CARTESIAN_POINT('Ctrl Pts',(-0.36301047494859,2.27424994956023,8.9017095986343));
#75946=CARTESIAN_POINT('Ctrl Pts',(-0.352420767781585,2.29478004505526,
8.85261753143099));
#75947=CARTESIAN_POINT('Ctrl Pts',(-0.349293930665851,2.3,8.82565270096287));
#75948=CARTESIAN_POINT('Ctrl Pts',(-0.349293930665851,2.3,8.77434729903714));
#75949=CARTESIAN_POINT('Ctrl Pts',(-0.352420767781585,2.29478004505526,
8.74738246856901));
#75950=CARTESIAN_POINT('Ctrl Pts',(-0.36301047494859,2.27424994956023,8.6982904013657));
#75951=CARTESIAN_POINT('Ctrl Pts',(-0.370257522731817,2.25895374562877,
8.67611103315415));
#75952=CARTESIAN_POINT('Ctrl Pts',(-0.383399376780438,2.22393542044062,
8.641092707966));
#75953=CARTESIAN_POINT('Ctrl Pts',(-0.390233771050516,2.20174032246956,
8.62576237805566));
#75954=CARTESIAN_POINT('Ctrl Pts',(-0.399836030760712,2.15257982613705,
8.60520470778352));
#75955=CARTESIAN_POINT('Ctrl Pts',(-0.4025,2.12558473189438,8.6));
#75956=CARTESIAN_POINT('Ctrl Pts',(-0.4025,2.1,8.6));
#75957=CARTESIAN_POINT('Origin',(-0.9,2.1,8.8));
#75958=CARTESIAN_POINT('',(0.349293930665851,1.9,8.8));
#75959=CARTESIAN_POINT('',(0.4025,2.1,9.));
#75960=CARTESIAN_POINT('Ctrl Pts',(0.349293930665851,1.9,8.8));
#75961=CARTESIAN_POINT('Ctrl Pts',(0.349293930665851,1.9,8.77434729903714));
#75962=CARTESIAN_POINT('Ctrl Pts',(0.352420767781585,1.90521995494474,8.74738246856901));
#75963=CARTESIAN_POINT('Ctrl Pts',(0.36301047494859,1.92575005043977,8.6982904013657));
#75964=CARTESIAN_POINT('Ctrl Pts',(0.370257522731817,1.94104625437123,8.67611103315415));
#75965=CARTESIAN_POINT('Ctrl Pts',(0.383399376780438,1.97606457955938,8.641092707966));
#75966=CARTESIAN_POINT('Ctrl Pts',(0.390233771050516,1.99825967753044,8.62576237805566));
#75967=CARTESIAN_POINT('Ctrl Pts',(0.399836030760712,2.04742017386295,8.60520470778352));
#75968=CARTESIAN_POINT('Ctrl Pts',(0.4025,2.07441526810562,8.6));
#75969=CARTESIAN_POINT('Ctrl Pts',(0.4025,2.12558473189438,8.6));
#75970=CARTESIAN_POINT('Ctrl Pts',(0.399836030760712,2.15257982613705,8.60520470778352));
#75971=CARTESIAN_POINT('Ctrl Pts',(0.390233771050516,2.20174032246956,8.62576237805566));
#75972=CARTESIAN_POINT('Ctrl Pts',(0.383399376780438,2.22393542044062,8.641092707966));
#75973=CARTESIAN_POINT('Ctrl Pts',(0.370257522731817,2.25895374562877,8.67611103315415));
#75974=CARTESIAN_POINT('Ctrl Pts',(0.36301047494859,2.27424994956023,8.6982904013657));
#75975=CARTESIAN_POINT('Ctrl Pts',(0.352420767781585,2.29478004505526,8.74738246856901));
#75976=CARTESIAN_POINT('Ctrl Pts',(0.349293930665851,2.3,8.77434729903714));
#75977=CARTESIAN_POINT('Ctrl Pts',(0.349293930665851,2.3,8.82565270096287));
#75978=CARTESIAN_POINT('Ctrl Pts',(0.352420767781585,2.29478004505526,8.85261753143099));
#75979=CARTESIAN_POINT('Ctrl Pts',(0.36301047494859,2.27424994956023,8.9017095986343));
#75980=CARTESIAN_POINT('Ctrl Pts',(0.370257522731817,2.25895374562877,8.92388896684585));
#75981=CARTESIAN_POINT('Ctrl Pts',(0.383399376780438,2.22393542044062,8.958907292034));
#75982=CARTESIAN_POINT('Ctrl Pts',(0.390233771050516,2.20174032246956,8.97423762194434));
#75983=CARTESIAN_POINT('Ctrl Pts',(0.399836030760712,2.15257982613705,8.99479529221648));
#75984=CARTESIAN_POINT('Ctrl Pts',(0.4025,2.12558473189438,9.));
#75985=CARTESIAN_POINT('Ctrl Pts',(0.4025,2.1,9.));
#75986=CARTESIAN_POINT('Ctrl Pts',(0.4025,2.1,9.));
#75987=CARTESIAN_POINT('Ctrl Pts',(0.4025,2.07441526810562,9.));
#75988=CARTESIAN_POINT('Ctrl Pts',(0.399836030760712,2.04742017386295,8.99479529221648));
#75989=CARTESIAN_POINT('Ctrl Pts',(0.390233771050516,1.99825967753044,8.97423762194434));
#75990=CARTESIAN_POINT('Ctrl Pts',(0.383399376780438,1.97606457955938,8.958907292034));
#75991=CARTESIAN_POINT('Ctrl Pts',(0.370257522731817,1.94104625437123,8.92388896684585));
#75992=CARTESIAN_POINT('Ctrl Pts',(0.36301047494859,1.92575005043977,8.9017095986343));
#75993=CARTESIAN_POINT('Ctrl Pts',(0.352420767781585,1.90521995494474,8.85261753143099));
#75994=CARTESIAN_POINT('Ctrl Pts',(0.349293930665851,1.9,8.82565270096286));
#75995=CARTESIAN_POINT('Ctrl Pts',(0.349293930665851,1.9,8.8));
#75996=CARTESIAN_POINT('',(0.9,2.1,9.));
#75997=CARTESIAN_POINT('',(-0.9,2.1,9.));
#75998=CARTESIAN_POINT('Origin',(0.9,2.1,8.8));
#75999=CARTESIAN_POINT('Origin',(0.,2.1,9.4));
#76000=CARTESIAN_POINT('',(-0.4025,2.1,9.4));
#76001=CARTESIAN_POINT('Origin',(0.,2.1,9.4));
#76002=CARTESIAN_POINT('',(-0.4025,2.1,9.4));
#76003=CARTESIAN_POINT('',(-0.4025,2.1,9.4));
#76004=CARTESIAN_POINT('',(-0.4025,2.1,6.));
#76005=CARTESIAN_POINT('',(-0.4025,2.1,9.4));
#76006=CARTESIAN_POINT('Origin',(0.,2.1,6.));
#76007=CARTESIAN_POINT('Origin',(0.,2.1,9.2));
#76008=CARTESIAN_POINT('',(-0.9,2.73245553203368,9.2));
#76009=CARTESIAN_POINT('',(-0.9,2.9,9.2));
#76010=CARTESIAN_POINT('',(-1.1,2.1,9.2));
#76011=CARTESIAN_POINT('Origin',(0.,2.1,9.2));
#76012=CARTESIAN_POINT('Origin',(0.,2.1,9.2));
#76013=CARTESIAN_POINT('Origin',(0.,2.1,9.2));
#76014=CARTESIAN_POINT('Origin',(0.,2.1,9.2));
#76015=CARTESIAN_POINT('Origin',(0.,2.1,9.2));
#76016=CARTESIAN_POINT('',(0.9,1.46754446796632,9.2));
#76017=CARTESIAN_POINT('',(0.9,1.3,9.2));
#76018=CARTESIAN_POINT('Origin',(0.,2.1,9.2));
#76019=CARTESIAN_POINT('Origin',(0.,2.1,9.2));
#76020=CARTESIAN_POINT('Origin',(0.,2.1,9.2));
#76021=CARTESIAN_POINT('Origin',(0.,2.1,9.2));
#76022=CARTESIAN_POINT('',(-1.1,2.1,9.4));
#76023=CARTESIAN_POINT('Origin',(0.,2.1,9.4));
#76024=CARTESIAN_POINT('',(-1.1,2.1,9.2));
#76025=CARTESIAN_POINT('Origin',(0.,2.1,9.2));
#76026=CARTESIAN_POINT('Origin',(0.,2.1,9.2));
#76027=CARTESIAN_POINT('Origin',(0.,2.1,9.4));
#76028=CARTESIAN_POINT('Origin',(0.,2.1,9.2));
#76029=CARTESIAN_POINT('',(0.9,1.3,9.2));
#76030=CARTESIAN_POINT('Origin',(0.,2.1,9.2));
#76031=CARTESIAN_POINT('',(-0.9,2.9,9.2));
#76032=CARTESIAN_POINT('Origin',(0.9,1.3,6.));
#76033=CARTESIAN_POINT('',(0.9,1.3,6.));
#76034=CARTESIAN_POINT('Origin',(-0.9,2.9,6.));
#76035=CARTESIAN_POINT('',(-0.9,2.9,6.));
#76036=CARTESIAN_POINT('Origin',(0.,2.1,6.));
#85756=UNCERTAINTY_MEASURE_WITH_UNIT(LENGTH_MEASURE(0.001),#85790,
'DISTANCE_ACCURACY_VALUE',
'Maximum model space distance between geometric entities at asserted c
onnectivities');
#85769=UNCERTAINTY_MEASURE_WITH_UNIT(LENGTH_MEASURE(0.001),#85790,
'DISTANCE_ACCURACY_VALUE',
'Maximum model space distance between geometric entities at asserted c
onnectivities');
#85776=(
GEOMETRIC_REPRESENTATION_CONTEXT(3)
GLOBAL_UNCERTAINTY_ASSIGNED_CONTEXT((#85756))
GLOBAL_UNIT_ASSIGNED_CONTEXT((#85790,#85792,#85793))
REPRESENTATION_CONTEXT('','3D')
);
#85789=(
GEOMETRIC_REPRESENTATION_CONTEXT(3)
GLOBAL_UNCERTAINTY_ASSIGNED_CONTEXT((#85769))
GLOBAL_UNIT_ASSIGNED_CONTEXT((#85790,#85792,#85793))
REPRESENTATION_CONTEXT('','3D')
);
#85790=(
LENGTH_UNIT()
NAMED_UNIT(*)
SI_UNIT(.CENTI.,.METRE.)
);
#85792=(
NAMED_UNIT(*)
PLANE_ANGLE_UNIT()
SI_UNIT($,.RADIAN.)
);
#85793=(
NAMED_UNIT(*)
SI_UNIT($,.STERADIAN.)
SOLID_ANGLE_UNIT()
);
#85800=SHAPE_DEFINITION_REPRESENTATION(#85819,#85868);
#85819=PRODUCT_DEFINITION_SHAPE('',$,#85888);
#85868=SHAPE_REPRESENTATION('',(#10504),#85776);
#85881=PRODUCT_DEFINITION_CONTEXT('part definition',#85940,'design');
#85888=PRODUCT_DEFINITION('Roller Carriage Spindle Nut',
'Roller Carriage Spindle Nut',#85907,#85881);
#85907=PRODUCT_DEFINITION_FORMATION('',$,#85948);
#85940=APPLICATION_CONTEXT(
'Core Data for Automotive Mechanical Design Process');
#85941=PRODUCT_CONTEXT('part definition',#85940,'mechanical');
#85948=PRODUCT('Roller Carriage Spindle Nut',
'Roller Carriage Spindle Nut',$,(#85941));
#85967=PRESENTATION_STYLE_ASSIGNMENT((#85985));
#85985=SURFACE_STYLE_USAGE(.BOTH.,#86003);
#86003=SURFACE_SIDE_STYLE('',(#86021));
#86021=SURFACE_STYLE_FILL_AREA(#86039);
#86039=FILL_AREA_STYLE('Opaque(200,203,207)',(#86057));
#86057=FILL_AREA_STYLE_COLOUR('Opaque(200,203,207)',#86075);
#86075=COLOUR_RGB('Opaque(200,203,207)', 0.09019608, 0.27058824, 0.51372549);
ENDSEC;
END-ISO-10303-21;
